ISO-10303-21;
HEADER;
/* Generated by software containing ST-Developer
 * from STEP Tools, Inc. (www.steptools.com) 
 */

FILE_DESCRIPTION(
/* description */ ('Turntable on roller ring'),
/* implementation_level */ '2;1');

FILE_NAME(
/* name */ 'Cap Screw - M4x16.step',
/* time_stamp */ '2026-10-28T03:23:59-07:00',
/* author */ (''),
/* organization */ (''),
/* preprocessor_version */ 'ST-DEVELOPER v20.2',
/* originating_system */ 'Autodesk Translation Framework v15.17.0.0',
/* authorisation */ '');

FILE_SCHEMA (('AUTOMOTIVE_DESIGN { 1 0 10303 214 3 1 1 }'));
ENDSEC;

DATA;
#10=MECHANICAL_DESIGN_GEOMETRIC_PRESENTATION_REPRESENTATION('',(#640),#16281);
#483=CONICAL_SURFACE('',#9471,0.325,0.785398163397448);
#484=CONICAL_SURFACE('',#9475,0.335,0.785398163397448);
#485=CONICAL_SURFACE('',#9479,0.21,0.463647609000806);
#486=CONICAL_SURFACE('',#9483,0.18,0.785398163397448);
#500=ORIENTED_CLOSED_SHELL('',*,#8383,.F.);
#504=BREP_WITH_VOIDS('Body1',#8382,(#500));
#521=SHAPE_REPRESENTATION_RELATIONSHIP('SRR','None',#16537,#576);
#576=ADVANCED_BREP_SHAPE_REPRESENTATION('',(#504),#16231);
#640=STYLED_ITEM('',(#16939),#504);
#865=FACE_BOUND('',#2049,.T.);
#1063=PLANE('',#9469);
#1064=PLANE('',#9477);
#1065=PLANE('',#9485);
#1066=PLANE('',#9486);
#1067=PLANE('',#9487);
#1068=PLANE('',#9488);
#1069=PLANE('',#9489);
#1070=PLANE('',#9490);
#1071=PLANE('',#9491);
#1072=PLANE('',#9492);
#1073=PLANE('',#9493);
#1431=FACE_OUTER_BOUND('',#2044,.T.);
#1432=FACE_OUTER_BOUND('',#2045,.T.);
#1433=FACE_OUTER_BOUND('',#2046,.T.);
#1434=FACE_OUTER_BOUND('',#2047,.T.);
#1435=FACE_OUTER_BOUND('',#2048,.T.);
#1436=FACE_OUTER_BOUND('',#2050,.T.);
#1437=FACE_OUTER_BOUND('',#2051,.T.);
#1438=FACE_OUTER_BOUND('',#2052,.T.);
#1439=FACE_OUTER_BOUND('',#2053,.T.);
#1440=FACE_OUTER_BOUND('',#2054,.T.);
#1441=FACE_OUTER_BOUND('',#2055,.T.);
#1442=FACE_OUTER_BOUND('',#2056,.T.);
#1443=FACE_OUTER_BOUND('',#2057,.T.);
#1444=FACE_OUTER_BOUND('',#2058,.T.);
#1445=FACE_OUTER_BOUND('',#2059,.T.);
#1446=FACE_OUTER_BOUND('',#2060,.T.);
#1447=FACE_OUTER_BOUND('',#2061,.T.);
#2044=EDGE_LOOP('',(#6431));
#2045=EDGE_LOOP('',(#6432,#6433,#6434,#6435));
#2046=EDGE_LOOP('',(#6436,#6437,#6438,#6439));
#2047=EDGE_LOOP('',(#6440,#6441,#6442,#6443));
#2048=EDGE_LOOP('',(#6444));
#2049=EDGE_LOOP('',(#6445));
#2050=EDGE_LOOP('',(#6446,#6447,#6448,#6449));
#2051=EDGE_LOOP('',(#6450,#6451,#6452,#6453));
#2052=EDGE_LOOP('',(#6454,#6455,#6456,#6457));
#2053=EDGE_LOOP('',(#6458));
#2054=EDGE_LOOP('',(#6459,#6460,#6461,#6462));
#2055=EDGE_LOOP('',(#6463,#6464,#6465,#6466));
#2056=EDGE_LOOP('',(#6467,#6468,#6469,#6470));
#2057=EDGE_LOOP('',(#6471,#6472,#6473,#6474));
#2058=EDGE_LOOP('',(#6475,#6476,#6477,#6478));
#2059=EDGE_LOOP('',(#6479,#6480,#6481,#6482));
#2060=EDGE_LOOP('',(#6483,#6484,#6485,#6486,#6487,#6488));
#2061=EDGE_LOOP('',(#6489,#6490,#6491,#6492,#6493,#6494));
#2641=LINE('',#14310,#3124);
#2642=LINE('',#14314,#3125);
#2643=LINE('',#14318,#3126);
#2644=LINE('',#14325,#3127);
#2645=LINE('',#14329,#3128);
#2646=LINE('',#14333,#3129);
#2647=LINE('',#14338,#3130);
#2648=LINE('',#14340,#3131);
#2649=LINE('',#14342,#3132);
#2650=LINE('',#14343,#3133);
#2651=LINE('',#14346,#3134);
#2652=LINE('',#14348,#3135);
#2653=LINE('',#14349,#3136);
#2654=LINE('',#14352,#3137);
#2655=LINE('',#14354,#3138);
#2656=LINE('',#14355,#3139);
#2657=LINE('',#14358,#3140);
#2658=LINE('',#14360,#3141);
#2659=LINE('',#14361,#3142);
#2660=LINE('',#14364,#3143);
#2661=LINE('',#14366,#3144);
#2662=LINE('',#14367,#3145);
#2663=LINE('',#14369,#3146);
#2664=LINE('',#14370,#3147);
#3124=VECTOR('',#11214,0.325);
#3125=VECTOR('',#11219,0.35);
#3126=VECTOR('',#11224,0.335);
#3127=VECTOR('',#11233,0.21);
#3128=VECTOR('',#11238,0.2);
#3129=VECTOR('',#11243,0.18);
#3130=VECTOR('',#11248,1.);
#3131=VECTOR('',#11249,1.);
#3132=VECTOR('',#11250,1.);
#3133=VECTOR('',#11251,1.);
#3134=VECTOR('',#11254,1.);
#3135=VECTOR('',#11255,1.);
#3136=VECTOR('',#11256,1.);
#3137=VECTOR('',#11259,1.);
#3138=VECTOR('',#11260,1.);
#3139=VECTOR('',#11261,1.);
#3140=VECTOR('',#11264,1.);
#3141=VECTOR('',#11265,1.);
#3142=VECTOR('',#11266,1.);
#3143=VECTOR('',#11269,1.);
#3144=VECTOR('',#11270,1.);
#3145=VECTOR('',#11271,1.);
#3146=VECTOR('',#11274,1.);
#3147=VECTOR('',#11275,1.);
#3683=CIRCLE('',#9470,0.3);
#3684=CIRCLE('',#9472,0.35);
#3685=CIRCLE('',#9474,0.35);
#3686=CIRCLE('',#9476,0.32);
#3687=CIRCLE('',#9478,0.22);
#3688=CIRCLE('',#9480,0.1954);
#3689=CIRCLE('',#9482,0.1954);
#3690=CIRCLE('',#9484,0.16);
#4215=VERTEX_POINT('',#14305);
#4216=VERTEX_POINT('',#14308);
#4217=VERTEX_POINT('',#14312);
#4218=VERTEX_POINT('',#14316);
#4219=VERTEX_POINT('',#14320);
#4220=VERTEX_POINT('',#14323);
#4221=VERTEX_POINT('',#14327);
#4222=VERTEX_POINT('',#14331);
#4223=VERTEX_POINT('',#14336);
#4224=VERTEX_POINT('',#14337);
#4225=VERTEX_POINT('',#14339);
#4226=VERTEX_POINT('',#14341);
#4227=VERTEX_POINT('',#14345);
#4228=VERTEX_POINT('',#14347);
#4229=VERTEX_POINT('',#14351);
#4230=VERTEX_POINT('',#14353);
#4231=VERTEX_POINT('',#14357);
#4232=VERTEX_POINT('',#14359);
#4233=VERTEX_POINT('',#14363);
#4234=VERTEX_POINT('',#14365);
#5026=EDGE_CURVE('',#4215,#4215,#3683,.T.);
#5027=EDGE_CURVE('',#4216,#4216,#3684,.T.);
#5028=EDGE_CURVE('',#4216,#4215,#2641,.T.);
#5029=EDGE_CURVE('',#4217,#4217,#3685,.T.);
#5030=EDGE_CURVE('',#4217,#4216,#2642,.T.);
#5031=EDGE_CURVE('',#4218,#4218,#3686,.T.);
#5032=EDGE_CURVE('',#4218,#4217,#2643,.T.);
#5033=EDGE_CURVE('',#4219,#4219,#3687,.T.);
#5034=EDGE_CURVE('',#4220,#4220,#3688,.F.);
#5035=EDGE_CURVE('',#4220,#4219,#2644,.T.);
#5036=EDGE_CURVE('',#4221,#4221,#3689,.F.);
#5037=EDGE_CURVE('',#4221,#4220,#2645,.T.);
#5038=EDGE_CURVE('',#4222,#4222,#3690,.T.);
#5039=EDGE_CURVE('',#4222,#4221,#2646,.T.);
#5040=EDGE_CURVE('',#4223,#4224,#2647,.T.);
#5041=EDGE_CURVE('',#4224,#4225,#2648,.T.);
#5042=EDGE_CURVE('',#4225,#4226,#2649,.T.);
#5043=EDGE_CURVE('',#4223,#4226,#2650,.T.);
#5044=EDGE_CURVE('',#4224,#4227,#2651,.T.);
#5045=EDGE_CURVE('',#4227,#4228,#2652,.T.);
#5046=EDGE_CURVE('',#4228,#4225,#2653,.T.);
#5047=EDGE_CURVE('',#4227,#4229,#2654,.T.);
#5048=EDGE_CURVE('',#4229,#4230,#2655,.T.);
#5049=EDGE_CURVE('',#4230,#4228,#2656,.T.);
#5050=EDGE_CURVE('',#4229,#4231,#2657,.T.);
#5051=EDGE_CURVE('',#4231,#4232,#2658,.T.);
#5052=EDGE_CURVE('',#4232,#4230,#2659,.T.);
#5053=EDGE_CURVE('',#4231,#4233,#2660,.T.);
#5054=EDGE_CURVE('',#4233,#4234,#2661,.T.);
#5055=EDGE_CURVE('',#4234,#4232,#2662,.T.);
#5056=EDGE_CURVE('',#4233,#4223,#2663,.T.);
#5057=EDGE_CURVE('',#4226,#4234,#2664,.T.);
#6431=ORIENTED_EDGE('',*,*,#5026,.F.);
#6432=ORIENTED_EDGE('',*,*,#5027,.F.);
#6433=ORIENTED_EDGE('',*,*,#5028,.T.);
#6434=ORIENTED_EDGE('',*,*,#5026,.T.);
#6435=ORIENTED_EDGE('',*,*,#5028,.F.);
#6436=ORIENTED_EDGE('',*,*,#5029,.F.);
#6437=ORIENTED_EDGE('',*,*,#5030,.T.);
#6438=ORIENTED_EDGE('',*,*,#5027,.T.);
#6439=ORIENTED_EDGE('',*,*,#5030,.F.);
#6440=ORIENTED_EDGE('',*,*,#5031,.F.);
#6441=ORIENTED_EDGE('',*,*,#5032,.T.);
#6442=ORIENTED_EDGE('',*,*,#5029,.T.);
#6443=ORIENTED_EDGE('',*,*,#5032,.F.);
#6444=ORIENTED_EDGE('',*,*,#5031,.T.);
#6445=ORIENTED_EDGE('',*,*,#5033,.F.);
#6446=ORIENTED_EDGE('',*,*,#5034,.F.);
#6447=ORIENTED_EDGE('',*,*,#5035,.T.);
#6448=ORIENTED_EDGE('',*,*,#5033,.T.);
#6449=ORIENTED_EDGE('',*,*,#5035,.F.);
#6450=ORIENTED_EDGE('',*,*,#5036,.F.);
#6451=ORIENTED_EDGE('',*,*,#5037,.T.);
#6452=ORIENTED_EDGE('',*,*,#5034,.T.);
#6453=ORIENTED_EDGE('',*,*,#5037,.F.);
#6454=ORIENTED_EDGE('',*,*,#5038,.F.);
#6455=ORIENTED_EDGE('',*,*,#5039,.T.);
#6456=ORIENTED_EDGE('',*,*,#5036,.T.);
#6457=ORIENTED_EDGE('',*,*,#5039,.F.);
#6458=ORIENTED_EDGE('',*,*,#5038,.T.);
#6459=ORIENTED_EDGE('',*,*,#5040,.T.);
#6460=ORIENTED_EDGE('',*,*,#5041,.T.);
#6461=ORIENTED_EDGE('',*,*,#5042,.T.);
#6462=ORIENTED_EDGE('',*,*,#5043,.F.);
#6463=ORIENTED_EDGE('',*,*,#5044,.T.);
#6464=ORIENTED_EDGE('',*,*,#5045,.T.);
#6465=ORIENTED_EDGE('',*,*,#5046,.T.);
#6466=ORIENTED_EDGE('',*,*,#5041,.F.);
#6467=ORIENTED_EDGE('',*,*,#5047,.T.);
#6468=ORIENTED_EDGE('',*,*,#5048,.T.);
#6469=ORIENTED_EDGE('',*,*,#5049,.T.);
#6470=ORIENTED_EDGE('',*,*,#5045,.F.);
#6471=ORIENTED_EDGE('',*,*,#5050,.T.);
#6472=ORIENTED_EDGE('',*,*,#5051,.T.);
#6473=ORIENTED_EDGE('',*,*,#5052,.T.);
#6474=ORIENTED_EDGE('',*,*,#5048,.F.);
#6475=ORIENTED_EDGE('',*,*,#5053,.T.);
#6476=ORIENTED_EDGE('',*,*,#5054,.T.);
#6477=ORIENTED_EDGE('',*,*,#5055,.T.);
#6478=ORIENTED_EDGE('',*,*,#5051,.F.);
#6479=ORIENTED_EDGE('',*,*,#5056,.T.);
#6480=ORIENTED_EDGE('',*,*,#5043,.T.);
#6481=ORIENTED_EDGE('',*,*,#5057,.T.);
#6482=ORIENTED_EDGE('',*,*,#5054,.F.);
#6483=ORIENTED_EDGE('',*,*,#5056,.F.);
#6484=ORIENTED_EDGE('',*,*,#5053,.F.);
#6485=ORIENTED_EDGE('',*,*,#5050,.F.);
#6486=ORIENTED_EDGE('',*,*,#5047,.F.);
#6487=ORIENTED_EDGE('',*,*,#5044,.F.);
#6488=ORIENTED_EDGE('',*,*,#5040,.F.);
#6489=ORIENTED_EDGE('',*,*,#5057,.F.);
#6490=ORIENTED_EDGE('',*,*,#5042,.F.);
#6491=ORIENTED_EDGE('',*,*,#5046,.F.);
#6492=ORIENTED_EDGE('',*,*,#5049,.F.);
#6493=ORIENTED_EDGE('',*,*,#5052,.F.);
#6494=ORIENTED_EDGE('',*,*,#5055,.F.);
#7750=CYLINDRICAL_SURFACE('',#9473,0.35);
#7751=CYLINDRICAL_SURFACE('',#9481,0.1954);
#8034=ADVANCED_FACE('',(#1431),#1063,.T.);
#8035=ADVANCED_FACE('',(#1432),#483,.T.);
#8036=ADVANCED_FACE('',(#1433),#7750,.T.);
#8037=ADVANCED_FACE('',(#1434),#484,.T.);
#8038=ADVANCED_FACE('',(#1435,#865),#1064,.T.);
#8039=ADVANCED_FACE('',(#1436),#485,.T.);
#8040=ADVANCED_FACE('',(#1437),#7751,.T.);
#8041=ADVANCED_FACE('',(#1438),#486,.T.);
#8042=ADVANCED_FACE('',(#1439),#1065,.T.);
#8043=ADVANCED_FACE('',(#1440),#1066,.F.);
#8044=ADVANCED_FACE('',(#1441),#1067,.F.);
#8045=ADVANCED_FACE('',(#1442),#1068,.F.);
#8046=ADVANCED_FACE('',(#1443),#1069,.F.);
#8047=ADVANCED_FACE('',(#1444),#1070,.F.);
#8048=ADVANCED_FACE('',(#1445),#1071,.F.);
#8049=ADVANCED_FACE('',(#1446),#1072,.F.);
#8050=ADVANCED_FACE('',(#1447),#1073,.F.);
#8382=CLOSED_SHELL('',(#8034,#8035,#8036,#8037,#8038,#8039,#8040,#8041,
#8042));
#8383=CLOSED_SHELL('',(#8043,#8044,#8045,#8046,#8047,#8048,#8049,#8050));
#9468=AXIS2_PLACEMENT_3D('',#14303,#11204,#11205);
#9469=AXIS2_PLACEMENT_3D('',#14304,#11206,#11207);
#9470=AXIS2_PLACEMENT_3D('',#14306,#11208,#11209);
#9471=AXIS2_PLACEMENT_3D('',#14307,#11210,#11211);
#9472=AXIS2_PLACEMENT_3D('',#14309,#11212,#11213);
#9473=AXIS2_PLACEMENT_3D('',#14311,#11215,#11216);
#9474=AXIS2_PLACEMENT_3D('',#14313,#11217,#11218);
#9475=AXIS2_PLACEMENT_3D('',#14315,#11220,#11221);
#9476=AXIS2_PLACEMENT_3D('',#14317,#11222,#11223);
#9477=AXIS2_PLACEMENT_3D('',#14319,#11225,#11226);
#9478=AXIS2_PLACEMENT_3D('',#14321,#11227,#11228);
#9479=AXIS2_PLACEMENT_3D('',#14322,#11229,#11230);
#9480=AXIS2_PLACEMENT_3D('',#14324,#11231,#11232);
#9481=AXIS2_PLACEMENT_3D('',#14326,#11234,#11235);
#9482=AXIS2_PLACEMENT_3D('',#14328,#11236,#11237);
#9483=AXIS2_PLACEMENT_3D('',#14330,#11239,#11240);
#9484=AXIS2_PLACEMENT_3D('',#14332,#11241,#11242);
#9485=AXIS2_PLACEMENT_3D('',#14334,#11244,#11245);
#9486=AXIS2_PLACEMENT_3D('',#14335,#11246,#11247);
#9487=AXIS2_PLACEMENT_3D('',#14344,#11252,#11253);
#9488=AXIS2_PLACEMENT_3D('',#14350,#11257,#11258);
#9489=AXIS2_PLACEMENT_3D('',#14356,#11262,#11263);
#9490=AXIS2_PLACEMENT_3D('',#14362,#11267,#11268);
#9491=AXIS2_PLACEMENT_3D('',#14368,#11272,#11273);
#9492=AXIS2_PLACEMENT_3D('',#14371,#11276,#11277);
#9493=AXIS2_PLACEMENT_3D('',#14372,#11278,#11279);
#11204=DIRECTION('axis',(0.,0.,1.));
#11205=DIRECTION('refdir',(1.,0.,0.));
#11206=DIRECTION('center_axis',(0.,1.,0.));
#11207=DIRECTION('ref_axis',(0.,0.,1.));
#11208=DIRECTION('center_axis',(0.,-1.,0.));
#11209=DIRECTION('ref_axis',(1.,0.,0.));
#11210=DIRECTION('center_axis',(0.,-1.,0.));
#11211=DIRECTION('ref_axis',(1.,0.,0.));
#11212=DIRECTION('center_axis',(0.,-1.,0.));
#11213=DIRECTION('ref_axis',(1.,0.,0.));
#11214=DIRECTION('',(0.707106781186547,0.707106781186548,8.65956056235493E-17));
#11215=DIRECTION('center_axis',(0.,-1.,0.));
#11216=DIRECTION('ref_axis',(1.,0.,0.));
#11217=DIRECTION('center_axis',(0.,-1.,0.));
#11218=DIRECTION('ref_axis',(1.,0.,0.));
#11219=DIRECTION('',(0.,1.,0.));
#11220=DIRECTION('center_axis',(0.,1.,0.));
#11221=DIRECTION('ref_axis',(1.,0.,0.));
#11222=DIRECTION('center_axis',(0.,-1.,0.));
#11223=DIRECTION('ref_axis',(1.,0.,0.));
#11224=DIRECTION('',(-0.707106781186547,0.707106781186548,-8.65956056235493E-17));
#11225=DIRECTION('center_axis',(0.,-1.,0.));
#11226=DIRECTION('ref_axis',(0.,0.,-1.));
#11227=DIRECTION('center_axis',(0.,-1.,0.));
#11228=DIRECTION('ref_axis',(1.,0.,0.));
#11229=DIRECTION('center_axis',(0.,1.,0.));
#11230=DIRECTION('ref_axis',(1.,0.,0.));
#11231=DIRECTION('center_axis',(0.,1.,0.));
#11232=DIRECTION('ref_axis',(1.,0.,0.));
#11233=DIRECTION('',(-0.447213595499958,0.894427190999916,-5.47678698264203E-17));
#11234=DIRECTION('center_axis',(0.,-1.,0.));
#11235=DIRECTION('ref_axis',(1.,0.,0.));
#11236=DIRECTION('center_axis',(0.,1.,0.));
#11237=DIRECTION('ref_axis',(1.,0.,0.));
#11238=DIRECTION('',(0.,1.,0.));
#11239=DIRECTION('center_axis',(0.,1.,0.));
#11240=DIRECTION('ref_axis',(1.,0.,0.));
#11241=DIRECTION('center_axis',(0.,-1.,0.));
#11242=DIRECTION('ref_axis',(1.,0.,0.));
#11243=DIRECTION('',(-0.707106781186547,0.707106781186548,-8.65956056235493E-17));
#11244=DIRECTION('center_axis',(0.,-1.,0.));
#11245=DIRECTION('ref_axis',(0.,0.,-1.));
#11246=DIRECTION('center_axis',(0.866025403784439,0.,-0.5));
#11247=DIRECTION('ref_axis',(0.5,0.,0.866025403784439));
#11248=DIRECTION('',(-0.5,0.,-0.866025403784439));
#11249=DIRECTION('',(0.,-1.,0.));
#11250=DIRECTION('',(0.5,0.,0.866025403784439));
#11251=DIRECTION('',(0.,-1.,0.));
#11252=DIRECTION('center_axis',(1.60246890531964E-16,0.,-1.));
#11253=DIRECTION('ref_axis',(1.,0.,1.60246890531964E-16));
#11254=DIRECTION('',(-1.,0.,-1.60246890531964E-16));
#11255=DIRECTION('',(0.,-1.,0.));
#11256=DIRECTION('',(1.,0.,1.60246890531964E-16));
#11257=DIRECTION('center_axis',(-0.866025403784439,0.,-0.5));
#11258=DIRECTION('ref_axis',(0.5,0.,-0.866025403784439));
#11259=DIRECTION('',(-0.5,0.,0.866025403784439));
#11260=DIRECTION('',(0.,-1.,0.));
#11261=DIRECTION('',(0.5,0.,-0.866025403784439));
#11262=DIRECTION('center_axis',(-0.866025403784439,0.,0.5));
#11263=DIRECTION('ref_axis',(-0.5,0.,-0.866025403784439));
#11264=DIRECTION('',(0.5,0.,0.866025403784439));
#11265=DIRECTION('',(0.,-1.,0.));
#11266=DIRECTION('',(-0.5,0.,-0.866025403784439));
#11267=DIRECTION('center_axis',(-1.60246890531964E-16,0.,1.));
#11268=DIRECTION('ref_axis',(-1.,0.,-1.60246890531964E-16));
#11269=DIRECTION('',(1.,0.,1.60246890531964E-16));
#11270=DIRECTION('',(0.,-1.,0.));
#11271=DIRECTION('',(-1.,0.,-1.60246890531964E-16));
#11272=DIRECTION('center_axis',(0.866025403784439,0.,0.5));
#11273=DIRECTION('ref_axis',(-0.5,0.,0.866025403784439));
#11274=DIRECTION('',(0.5,0.,-0.866025403784439));
#11275=DIRECTION('',(-0.5,0.,0.866025403784439));
#11276=DIRECTION('center_axis',(0.,1.,0.));
#11277=DIRECTION('ref_axis',(1.,0.,0.));
#11278=DIRECTION('center_axis',(0.,-1.,0.));
#11279=DIRECTION('ref_axis',(0.,0.,-1.));
#14303=CARTESIAN_POINT('',(0.,0.,0.));
#14304=CARTESIAN_POINT('Origin',(0.3,0.4,0.));
#14305=CARTESIAN_POINT('',(-0.3,0.4,-3.67394039744206E-17));
#14306=CARTESIAN_POINT('Origin',(0.,0.4,0.));
#14307=CARTESIAN_POINT('Origin',(0.,0.375,0.));
#14308=CARTESIAN_POINT('',(-0.35,0.35,-4.28626379701573E-17));
#14309=CARTESIAN_POINT('Origin',(0.,0.35,0.));
#14310=CARTESIAN_POINT('',(-0.325,0.375,-3.9801020972289E-17));
#14311=CARTESIAN_POINT('Origin',(0.,0.19,0.));
#14312=CARTESIAN_POINT('',(-0.35,0.03,-4.28626379701574E-17));
#14313=CARTESIAN_POINT('Origin',(0.,0.03,0.));
#14314=CARTESIAN_POINT('',(-0.35,0.19,-4.28626379701574E-17));
#14315=CARTESIAN_POINT('Origin',(0.,0.0149999999999999,0.));
#14316=CARTESIAN_POINT('',(-0.32,-3.29597460435593E-17,-3.91886975727153E-17));
#14317=CARTESIAN_POINT('Origin',(0.,0.,0.));
#14318=CARTESIAN_POINT('',(-0.335,0.0149999999999999,-4.10256677714363E-17));
#14319=CARTESIAN_POINT('Origin',(0.22,0.,0.));
#14320=CARTESIAN_POINT('',(-0.22,-6.93889390390723E-18,-2.69422295812418E-17));
#14321=CARTESIAN_POINT('Origin',(0.,0.,0.));
#14322=CARTESIAN_POINT('Origin',(0.,-0.02,0.));
#14323=CARTESIAN_POINT('',(-0.1954,-0.0492,2.39295984553393E-17));
#14324=CARTESIAN_POINT('Origin',(0.,-0.0492,0.));
#14325=CARTESIAN_POINT('',(-0.21,-0.02,-2.57175827820944E-17));
#14326=CARTESIAN_POINT('Origin',(0.,-0.8,0.));
#14327=CARTESIAN_POINT('',(-0.1954,-1.5646,2.39295984553393E-17));
#14328=CARTESIAN_POINT('Origin',(0.,-1.5646,0.));
#14329=CARTESIAN_POINT('',(-0.1954,-0.8,-2.39295984553393E-17));
#14330=CARTESIAN_POINT('Origin',(0.,-1.58,0.));
#14331=CARTESIAN_POINT('',(-0.16,-1.6,-1.95943487863577E-17));
#14332=CARTESIAN_POINT('Origin',(0.,-1.6,0.));
#14333=CARTESIAN_POINT('',(-0.18,-1.58,-2.20436423846524E-17));
#14334=CARTESIAN_POINT('Origin',(0.,-1.6,0.));
#14335=CARTESIAN_POINT('Origin',(0.0866025403784439,-0.4,-0.15));
#14336=CARTESIAN_POINT('',(0.173205080756888,-0.4,0.));
#14337=CARTESIAN_POINT('',(0.0866025403784439,-0.4,-0.15));
#14338=CARTESIAN_POINT('',(0.173205080756888,-0.4,0.));
#14339=CARTESIAN_POINT('',(0.0866025403784439,-0.64,-0.15));
#14340=CARTESIAN_POINT('',(0.0866025403784439,-0.4,-0.15));
#14341=CARTESIAN_POINT('',(0.173205080756888,-0.64,0.));
#14342=CARTESIAN_POINT('',(0.173205080756888,-0.64,0.));
#14343=CARTESIAN_POINT('',(0.173205080756888,-0.4,0.));
#14344=CARTESIAN_POINT('Origin',(-0.0866025403784438,-0.4,-0.15));
#14345=CARTESIAN_POINT('',(-0.0866025403784438,-0.4,-0.15));
#14346=CARTESIAN_POINT('',(0.0866025403784439,-0.4,-0.15));
#14347=CARTESIAN_POINT('',(-0.0866025403784438,-0.64,-0.15));
#14348=CARTESIAN_POINT('',(-0.0866025403784438,-0.4,-0.15));
#14349=CARTESIAN_POINT('',(0.0866025403784439,-0.64,-0.15));
#14350=CARTESIAN_POINT('Origin',(-0.173205080756888,-0.4,-2.77555756156289E-17));
#14351=CARTESIAN_POINT('',(-0.173205080756888,-0.4,-2.12115047744981E-17));
#14352=CARTESIAN_POINT('',(-0.0866025403784438,-0.4,-0.15));
#14353=CARTESIAN_POINT('',(-0.173205080756888,-0.64,-2.77555756156289E-17));
#14354=CARTESIAN_POINT('',(-0.173205080756888,-0.4,-2.12115047744981E-17));
#14355=CARTESIAN_POINT('',(-0.0866025403784438,-0.64,-0.15));
#14356=CARTESIAN_POINT('Origin',(-0.0866025403784439,-0.4,0.15));
#14357=CARTESIAN_POINT('',(-0.0866025403784439,-0.4,0.15));
#14358=CARTESIAN_POINT('',(-0.173205080756888,-0.4,-2.12115047744981E-17));
#14359=CARTESIAN_POINT('',(-0.0866025403784439,-0.64,0.15));
#14360=CARTESIAN_POINT('',(-0.0866025403784439,-0.4,0.15));
#14361=CARTESIAN_POINT('',(-0.173205080756888,-0.64,-2.12115047744981E-17));
#14362=CARTESIAN_POINT('Origin',(0.0866025403784439,-0.4,0.15));
#14363=CARTESIAN_POINT('',(0.0866025403784439,-0.4,0.15));
#14364=CARTESIAN_POINT('',(-0.0866025403784439,-0.4,0.15));
#14365=CARTESIAN_POINT('',(0.0866025403784439,-0.64,0.15));
#14366=CARTESIAN_POINT('',(0.0866025403784439,-0.4,0.15));
#14367=CARTESIAN_POINT('',(-0.0866025403784439,-0.64,0.15));
#14368=CARTESIAN_POINT('Origin',(0.173205080756888,-0.4,0.));
#14369=CARTESIAN_POINT('',(0.0866025403784439,-0.4,0.15));
#14370=CARTESIAN_POINT('',(0.0866025403784439,-0.64,0.15));
#14371=CARTESIAN_POINT('Origin',(0.,-0.4,-2.77555756156289E-17));
#14372=CARTESIAN_POINT('Origin',(0.,-0.64,-2.77555756156289E-17));
#16162=UNCERTAINTY_MEASURE_WITH_UNIT(LENGTH_MEASURE(0.001),#16282,
'DISTANCE_ACCURACY_VALUE',
'Maximum model space distance between geometric entities at asserted c
onnectivities');
#16212=UNCERTAINTY_MEASURE_WITH_UNIT(LENGTH_MEASURE(0.001),#16282,
'DISTANCE_ACCURACY_VALUE',
'Maximum model space distance between geometric entities at asserted c
onnectivities');
#16231=(
GEOMETRIC_REPRESENTATION_CONTEXT(3)
GLOBAL_UNCERTAINTY_ASSIGNED_CONTEXT((#16162))
GLOBAL_UNIT_ASSIGNED_CONTEXT((#16282,#16284,#16285))
REPRESENTATION_CONTEXT('','3D')
);
#16281=(
GEOMETRIC_REPRESENTATION_CONTEXT(3)
GLOBAL_UNCERTAINTY_ASSIGNED_CONTEXT((#16212))
GLOBAL_UNIT_ASSIGNED_CONTEXT((#16282,#16284,#16285))
REPRESENTATION_CONTEXT('','3D')
);
#16282=(
LENGTH_UNIT()
NAMED_UNIT(*)
SI_UNIT(.CENTI.,.METRE.)
);
#16284=(
NAMED_UNIT(*)
PLANE_ANGLE_UNIT()
SI_UNIT($,.RADIAN.)
);
#16285=(
NAMED_UNIT(*)
SI_UNIT($,.STERADIAN.)
SOLID_ANGLE_UNIT()
);
#16304=SHAPE_DEFINITION_REPRESENTATION(#16377,#16537);
#16377=PRODUCT_DEFINITION_SHAPE('',$,#16606);
#16537=SHAPE_REPRESENTATION('',(#9468),#16231);
#16587=PRODUCT_DEFINITION_CONTEXT('part definition',#16793,'design');
#16606=PRODUCT_DEFINITION('Cap Screw - M4x16','Cap Screw - M4x16',#16674,
#16587);
#16674=PRODUCT_DEFINITION_FORMATION('',$,#16813);
#16793=APPLICATION_CONTEXT(
'Core Data for Automotive Mechanical Design Process');
#16794=PRODUCT_CONTEXT('part definition',#16793,'mechanical');
#16813=PRODUCT('Cap Screw - M4x16','Cap Screw - M4x16',
'Cap Screw - M4x16',(#16794));
#16933=COLOUR_RGB('Black',0.12,0.14,0.17);
#16934=FILL_AREA_STYLE_COLOUR('',#16933);
#16935=FILL_AREA_STYLE('',(#16934));
#16936=SURFACE_STYLE_FILL_AREA(#16935);
#16937=SURFACE_SIDE_STYLE('',(#16936));
#16938=SURFACE_STYLE_USAGE(.BOTH.,#16937);
#16939=PRESENTATION_STYLE_ASSIGNMENT((#16938));
ENDSEC;
END-ISO-10303-21;
